ISO-10303-21;
HEADER;
FILE_DESCRIPTION (('STEP AP203'),
    '1' );
FILE_NAME ('Aloris-BXA-Handle-Rod.step',
    '2026-10-07T20:09:13',
    ( '' ),
    ( '' ),
    'SwSTEP 2.0',
    'SolidWorks 2024',
    '' );
FILE_SCHEMA (( 'AUTOMOTIVE_DESIGN' ));
ENDSEC;

DATA;
#17=AXIS2_PLACEMENT_3D ( 'NONE', #19179, #8074, #22716 ) ;
#18=FACE_OUTER_BOUND ( 'NONE', #649, .T. ) ;
#104=CARTESIAN_POINT ( 'NONE',  ( 0.000000000000000000, 5.501232050807569607, 0.000000000000000000 ) ) ;
#113=LINE ( 'NONE', #7555, #14963 ) ;
#139=DIRECTION ( 'NONE',  ( 0.000000000000000000, -1.000000000000000000, -0.000000000000000000 ) ) ;
#188=ORIENTED_EDGE ( 'NONE', *, *, #16033, .F. ) ;
#192=ORIENTED_EDGE ( 'NONE', *, *, #14503, .T. ) ;
#214=CARTESIAN_POINT ( 'NONE',  ( 0.000000000000000000, 0.000000000000000000, 0.000000000000000000 ) ) ;
#231=ORIENTED_EDGE ( 'NONE', *, *, #20196, .T. ) ;
#310=CARTESIAN_POINT ( 'NONE',  ( 0.000000000000000000, 0.000000000000000000, 0.2041999999999999926 ) ) ;
#395=CARTESIAN_POINT ( 'NONE',  ( 3.062437355670495042E-17, 0.4202679491924311561, -0.2499999999999999722 ) ) ;
#404=VERTEX_POINT ( 'NONE', #21099 ) ;
#406=CIRCLE ( 'NONE', #20276, 0.001000000000000003057 ) ;
#409=VERTEX_POINT ( 'NONE', #19265 ) ;
#460=CARTESIAN_POINT ( 'NONE',  ( 0.000000000000000000, 5.580000000000000959, -0.2500000000000000555 ) ) ;
#515=DIRECTION ( 'NONE',  ( 0.000000000000000000, 0.000000000000000000, 1.000000000000000000 ) ) ;
#535=DIRECTION ( 'NONE',  ( 0.000000000000000000, 0.000000000000000000, 1.000000000000000000 ) ) ;
#563=EDGE_LOOP ( 'NONE', ( #5895, #19879, #20173, #15118 ) ) ;
#612=EDGE_CURVE ( 'NONE', #20185, #20917, #15444, .T. ) ;
#622=DIRECTION ( 'NONE',  ( -0.000000000000000000, 1.000000000000000000, -0.000000000000000000 ) ) ;
#649=EDGE_LOOP ( 'NONE', ( #2562, #20892, #11863, #14301 ) ) ;
#659=AXIS2_PLACEMENT_3D ( 'NONE', #4875, #17930, #1226 ) ;
#704=UNCERTAINTY_MEASURE_WITH_UNIT (LENGTH_MEASURE( 1.000000000000000082E-05 ), #17589, 'distance_accuracy_value', 'NONE');
#743=CARTESIAN_POINT ( 'NONE',  ( 0.000000000000000000, 6.000000000000000888, -0.2500000000000000000 ) ) ;
#747=DIRECTION ( 'NONE',  ( -0.000000000000000000, -1.000000000000000000, -0.000000000000000000 ) ) ;
#778=AXIS2_PLACEMENT_3D ( 'NONE', #4712, #11939, #2766 ) ;
#783=DIRECTION ( 'NONE',  ( 0.000000000000000000, 0.000000000000000000, 1.000000000000000000 ) ) ;
#790=EDGE_LOOP ( 'NONE', ( #12525, #8590 ) ) ;
#871=ADVANCED_FACE ( 'NONE', ( #2795 ), #8408, .F. ) ;
#947=EDGE_LOOP ( 'NONE', ( #11967, #15478, #188, #18609 ) ) ;
#997=ORIENTED_EDGE ( 'NONE', *, *, #3467, .T. ) ;
#1026=AXIS2_PLACEMENT_3D ( 'NONE', #11287, #7737, #9571 ) ;
#1122=ADVANCED_FACE ( 'NONE', ( #8242 ), #12339, .F. ) ;
#1166=ORIENTED_EDGE ( 'NONE', *, *, #22138, .T. ) ;
#1189=ORIENTED_EDGE ( 'NONE', *, *, #612, .F. ) ;
#1190=CIRCLE ( 'NONE', #7429, 0.001000000000000037101 ) ;
#1212=CARTESIAN_POINT ( 'NONE',  ( 0.000000000000000000, 5.579732050807569621, 0.000000000000000000 ) ) ;
#1226=DIRECTION ( 'NONE',  ( 0.000000000000000000, 0.000000000000000000, 1.000000000000000000 ) ) ;
#1233=DIRECTION ( 'NONE',  ( 6.123233995738605068E-17, -0.8660254037843519992, 0.5000000000001502132 ) ) ;
#1281=CARTESIAN_POINT ( 'NONE',  ( 0.000000000000000000, 5.500232050807569273, 0.000000000000000000 ) ) ;
#1299=DIRECTION ( 'NONE',  ( 0.000000000000000000, 0.000000000000000000, 1.000000000000000000 ) ) ;
#1305=DIRECTION ( 'NONE',  ( 0.000000000000000000, 0.000000000000000000, 1.000000000000000000 ) ) ;
#1306=CIRCLE ( 'NONE', #3636, 0.2500000000000000555 ) ;
#1370=ORIENTED_EDGE ( 'NONE', *, *, #18301, .T. ) ;
#1396=ORIENTED_EDGE ( 'NONE', *, *, #15440, .T. ) ;
#1433=EDGE_LOOP ( 'NONE', ( #3290, #23860, #7001, #1189 ) ) ;
#1470=ORIENTED_EDGE ( 'NONE', *, *, #18257, .F. ) ;
#1570=ORIENTED_EDGE ( 'NONE', *, *, #23902, .T. ) ;
#1594=CARTESIAN_POINT ( 'NONE',  ( 0.000000000000000000, 0.4997679491924311157, 0.2510000000000000009 ) ) ;
#1659=EDGE_CURVE ( 'NONE', #409, #2709, #12359, .T. ) ;
#1686=VERTEX_POINT ( 'NONE', #16377 ) ;
#1735=DIRECTION ( 'NONE',  ( 0.000000000000000000, 0.000000000000000000, 1.000000000000000000 ) ) ;
#1796=DIRECTION ( 'NONE',  ( 0.000000000000000000, 0.000000000000000000, 1.000000000000000000 ) ) ;
#1823=DIRECTION ( 'NONE',  ( -0.000000000000000000, -1.000000000000000000, -0.000000000000000000 ) ) ;
#1859=EDGE_CURVE ( 'NONE', #13713, #9037, #17449, .T. ) ;
#1962=DIRECTION ( 'NONE',  ( 0.000000000000000000, 0.000000000000000000, 1.000000000000000000 ) ) ;
#1991=ORIENTED_EDGE ( 'NONE', *, *, #22138, .F. ) ;
#1997=TOROIDAL_SURFACE ( 'NONE', #13311, 0.2510000000000000009, 0.001000000000000037101 ) ;
#2015=CARTESIAN_POINT ( 'NONE',  ( 0.000000000000000000, 0.000000000000000000, 0.000000000000000000 ) ) ;
#2041=AXIS2_PLACEMENT_3D ( 'NONE', #15572, #9607, #22995 ) ;
#2071=VECTOR ( 'NONE', #22271, 39.37007874015748143 ) ;
#2076=ORIENTED_EDGE ( 'NONE', *, *, #8881, .T. ) ;
#2142=EDGE_CURVE ( 'NONE', #12951, #404, #11183, .T. ) ;
#2204=AXIS2_PLACEMENT_3D ( 'NONE', #10215, #8851, #1299 ) ;
#2238=CIRCLE ( 'NONE', #5338, 0.2041999999999999926 ) ;
#2257=VERTEX_POINT ( 'NONE', #9139 ) ;
#2271=ORIENTED_EDGE ( 'NONE', *, *, #6162, .F. ) ;
#2420=ADVANCED_FACE ( 'NONE', ( #22300 ), #5597, .T. ) ;
#2445=ORIENTED_EDGE ( 'NONE', *, *, #19287, .T. ) ;
#2462=DIRECTION ( 'NONE',  ( 0.000000000000000000, 1.000000000000000000, 0.000000000000000000 ) ) ;
#2484=CIRCLE ( 'NONE', #18051, 0.001000000000000003057 ) ;
#2492=EDGE_LOOP ( 'NONE', ( #5141, #6398, #19661, #6485 ) ) ;
#2515=FACE_OUTER_BOUND ( 'NONE', #12471, .T. ) ;
#2562=ORIENTED_EDGE ( 'NONE', *, *, #20311, .T. ) ;
#2569=CYLINDRICAL_SURFACE ( 'NONE', #16931, 0.2499999999999999722 ) ;
#2586=CARTESIAN_POINT ( 'NONE',  ( 3.073863465859856523E-17, 0.4202679491924311006, -0.2510000000000000009 ) ) ;
#2656=APPLICATION_CONTEXT ( 'configuration controlled 3d designs of mechanical parts and assemblies' ) ;
#2678=EDGE_LOOP ( 'NONE', ( #4352, #6182, #1396, #22973 ) ) ;
#2690=DIRECTION ( 'NONE',  ( 0.000000000000000000, -0.7071067811865376918, -0.7071067811865573427 ) ) ;
#2692=DIRECTION ( 'NONE',  ( 1.224646799147316476E-16, 0.000000000000000000, -1.000000000000000000 ) ) ;
#2693=AXIS2_PLACEMENT_3D ( 'NONE', #3759, #16921, #783 ) ;
#2709=VERTEX_POINT ( 'NONE', #17657 ) ;
#2728=AXIS2_PLACEMENT_3D ( 'NONE', #3771, #18642, #14511 ) ;
#2746=ORIENTED_EDGE ( 'NONE', *, *, #21858, .T. ) ;
#2766=DIRECTION ( 'NONE',  ( 0.000000000000000000, 0.000000000000000000, -1.000000000000000000 ) ) ;
#2795=FACE_OUTER_BOUND ( 'NONE', #17143, .T. ) ;
#2841=DIRECTION ( 'NONE',  ( 0.000000000000000000, 0.000000000000000000, 1.000000000000000000 ) ) ;
#2851=VERTEX_POINT ( 'NONE', #16138 ) ;
#2897=EDGE_CURVE ( 'NONE', #17212, #9355, #18589, .T. ) ;
#2899=CARTESIAN_POINT ( 'NONE',  ( 3.827021247335479543E-17, 5.500232050807569273, 0.3125000000000001665 ) ) ;
#2923=CARTESIAN_POINT ( 'NONE',  ( 0.000000000000000000, 6.000000000000000888, -0.2041999999999999926 ) ) ;
#2932=CARTESIAN_POINT ( 'NONE',  ( 0.000000000000000000, 6.000000000000000888, 0.000000000000000000 ) ) ;
#2962=CARTESIAN_POINT ( 'NONE',  ( 3.061616997868383018E-17, 0.000000000000000000, -0.2500000000000000000 ) ) ;
#2977=APPLICATION_CONTEXT ( 'configuration controlled 3d designs of mechanical parts and assemblies' ) ;
#2997=LINE ( 'NONE', #10447, #8911 ) ;
#3011=ORIENTED_EDGE ( 'NONE', *, *, #19414, .T. ) ;
#3118=DIRECTION ( 'NONE',  ( 0.000000000000000000, -1.000000000000000000, 0.000000000000000000 ) ) ;
#3204=DIRECTION ( 'NONE',  ( 0.000000000000000000, 0.000000000000000000, -1.000000000000000000 ) ) ;
#3208=ADVANCED_FACE ( 'NONE', ( #7173 ), #11198, .T. ) ;
#3290=ORIENTED_EDGE ( 'NONE', *, *, #19171, .F. ) ;
#3323=DIRECTION ( 'NONE',  ( -0.000000000000000000, 1.000000000000000000, -0.000000000000000000 ) ) ;
#3326=LINE ( 'NONE', #18569, #12188 ) ;
#3467=EDGE_CURVE ( 'NONE', #9682, #22114, #2238, .T. ) ;
#3476=EDGE_LOOP ( 'NONE', ( #11159, #7890, #23737, #10078 ) ) ;
#3517=CARTESIAN_POINT ( 'NONE',  ( 3.061616997868382402E-17, 6.000000000000000888, 0.2499999999999999722 ) ) ;
#3536=CARTESIAN_POINT ( 'NONE',  ( 0.000000000000000000, 5.501232050807569607, 0.000000000000000000 ) ) ;
#3554=CARTESIAN_POINT ( 'NONE',  ( 0.000000000000000000, 0.4199999999999998734, 0.000000000000000000 ) ) ;
#3634=CARTESIAN_POINT ( 'NONE',  ( 0.000000000000000000, 0.4202679491924311006, 0.000000000000000000 ) ) ;
#3636=AXIS2_PLACEMENT_3D ( 'NONE', #3554, #11005, #18433 ) ;
#3642=CARTESIAN_POINT ( 'NONE',  ( 0.000000000000000000, 6.000000000000000888, 0.000000000000000000 ) ) ;
#3670=VECTOR ( 'NONE', #3942, 39.37007874015748854 ) ;
#3759=CARTESIAN_POINT ( 'NONE',  ( 0.2510000000000000009, 0.4997679491924311157, 0.000000000000000000 ) ) ;
#3771=CARTESIAN_POINT ( 'NONE',  ( 0.000000000000000000, 5.579732050807569621, 0.000000000000000000 ) ) ;
#3898=ORIENTED_EDGE ( 'NONE', *, *, #15758, .T. ) ;
#3899=DIRECTION ( 'NONE',  ( 0.000000000000000000, 0.000000000000000000, -1.000000000000000000 ) ) ;
#3925=FACE_BOUND ( 'NONE', #15227, .T. ) ;
#3928=EDGE_CURVE ( 'NONE', #14964, #2709, #17830, .T. ) ;
#3930=CONICAL_SURFACE ( 'NONE', #17558, 0.2041999999999999926, 0.7853981633974621568 ) ;
#3942=DIRECTION ( 'NONE',  ( 8.659560562355001884E-17, 0.7071067811865416886, -0.7071067811865531239 ) ) ;
#3987=DIRECTION ( 'NONE',  ( 0.000000000000000000, 0.000000000000000000, 1.000000000000000000 ) ) ;
#4158=ORIENTED_EDGE ( 'NONE', *, *, #15111, .F. ) ;
#4264=DIRECTION ( 'NONE',  ( -0.000000000000000000, 1.000000000000000000, -0.000000000000000000 ) ) ;
#4272=DIRECTION ( 'NONE',  ( 0.000000000000000000, 0.000000000000000000, -1.000000000000000000 ) ) ;
#4352=ORIENTED_EDGE ( 'NONE', *, *, #20196, .F. ) ;
#4369=EDGE_LOOP ( 'NONE', ( #14695, #21279, #17997, #18660 ) ) ;
#4416=DIRECTION ( 'NONE',  ( -0.000000000000000000, -1.000000000000000000, -0.000000000000000000 ) ) ;
#4418=EDGE_LOOP ( 'NONE', ( #22676, #17249, #6262, #14209 ) ) ;
#4448=AXIS2_PLACEMENT_3D ( 'NONE', #6000, #11267, #515 ) ;
#4493=PRODUCT_DEFINITION_FORMATION_WITH_SPECIFIED_SOURCE ( 'ANY', '', #7006, .NOT_KNOWN. ) ;
#4510=DIRECTION ( 'NONE',  ( -0.000000000000000000, -1.000000000000000000, -0.000000000000000000 ) ) ;
#4537=DIRECTION ( 'NONE',  ( 0.000000000000000000, 0.000000000000000000, -1.000000000000000000 ) ) ;
#4549=ORIENTED_EDGE ( 'NONE', *, *, #9313, .T. ) ;
#4652=ORIENTED_EDGE ( 'NONE', *, *, #11311, .F. ) ;
#4712=CARTESIAN_POINT ( 'NONE',  ( 0.000000000000000000, 5.579732050807569621, 0.000000000000000000 ) ) ;
#4727=DIRECTION ( 'NONE',  ( -0.000000000000000000, -1.000000000000000000, -0.000000000000000000 ) ) ;
#4753=CARTESIAN_POINT ( 'NONE',  ( 0.000000000000000000, 5.500232050807569273, -0.3125000000000001665 ) ) ;
#4761=VERTEX_POINT ( 'NONE', #23496 ) ;
#4809=AXIS2_PLACEMENT_3D ( 'NONE', #19279, #8298, #6471 ) ;
#4813=DIRECTION ( 'NONE',  ( 0.000000000000000000, 0.000000000000000000, -1.000000000000000000 ) ) ;
#4831=EDGE_CURVE ( 'NONE', #13516, #22476, #18632, .T. ) ;
#4875=CARTESIAN_POINT ( 'NONE',  ( 0.000000000000000000, 0.4997679491924311157, 0.000000000000000000 ) ) ;
#4902=CIRCLE ( 'NONE', #8798, 0.3125000000000001665 ) ;
#4966=LINE ( 'NONE', #21914, #13748 ) ;
#5023=DIRECTION ( 'NONE',  ( -0.000000000000000000, 1.000000000000000000, -0.000000000000000000 ) ) ;
#5043=EDGE_LOOP ( 'NONE', ( #15172, #22124, #192, #21212 ) ) ;
#5098=AXIS2_PLACEMENT_3D ( 'NONE', #23429, #10419, #15888 ) ;
#5141=ORIENTED_EDGE ( 'NONE', *, *, #6540, .F. ) ;
#5149=CARTESIAN_POINT ( 'NONE',  ( 0.000000000000000000, 0.4199999999999998734, 0.000000000000000000 ) ) ;
#5268=DIRECTION ( 'NONE',  ( -0.000000000000000000, 1.000000000000000000, -0.000000000000000000 ) ) ;
#5282=EDGE_LOOP ( 'NONE', ( #7962, #19382, #1370, #6304 ) ) ;
#5290=ADVANCED_FACE ( 'NONE', ( #2515 ), #23284, .F. ) ;
#5319=ORIENTED_EDGE ( 'NONE', *, *, #17365, .F. ) ;
#5326=LINE ( 'NONE', #5447, #2071 ) ;
#5338=AXIS2_PLACEMENT_3D ( 'NONE', #214, #18872, #5938 ) ;
#5360=ORIENTED_EDGE ( 'NONE', *, *, #13525, .T. ) ;
#5371=ORIENTED_EDGE ( 'NONE', *, *, #19009, .T. ) ;
#5433=DIRECTION ( 'NONE',  ( -0.000000000000000000, -1.000000000000000000, -0.000000000000000000 ) ) ;
#5447=CARTESIAN_POINT ( 'NONE',  ( 0.000000000000000000, 0.000000000000000000, 0.2500000000000000000 ) ) ;
#5469=FACE_OUTER_BOUND ( 'NONE', #15841, .T. ) ;
#5593=DIRECTION ( 'NONE',  ( 0.000000000000000000, 0.000000000000000000, -1.000000000000000000 ) ) ;
#5597=CYLINDRICAL_SURFACE ( 'NONE', #11575, 0.3125000000000000555 ) ;
#5635=EDGE_CURVE ( 'NONE', #9355, #17212, #16671, .T. ) ;
#5779=ORIENTED_EDGE ( 'NONE', *, *, #8881, .F. ) ;
#5871=VERTEX_POINT ( 'NONE', #10416 ) ;
#5895=ORIENTED_EDGE ( 'NONE', *, *, #1659, .F. ) ;
#5913=ORIENTED_EDGE ( 'NONE', *, *, #2897, .T. ) ;
#5920=CARTESIAN_POINT ( 'NONE',  ( 0.000000000000000000, 6.000000000000000888, -0.2041999999999999926 ) ) ;
#5938=DIRECTION ( 'NONE',  ( 0.000000000000000000, 0.000000000000000000, 1.000000000000000000 ) ) ;
#5945=ORIENTED_EDGE ( 'NONE', *, *, #19344, .T. ) ;
#6000=CARTESIAN_POINT ( 'NONE',  ( 0.000000000000000000, 0.4199999999999998734, 0.000000000000000000 ) ) ;
#6022=DIRECTION ( 'NONE',  ( 0.000000000000000000, 0.000000000000000000, 1.000000000000000000 ) ) ;
#6143=CARTESIAN_POINT ( 'NONE',  ( 0.000000000000000000, 5.580000000000000959, 0.000000000000000000 ) ) ;
#6150=AXIS2_PLACEMENT_3D ( 'NONE', #7135, #16405, #20414 ) ;
#6162=EDGE_CURVE ( 'NONE', #4761, #17737, #7744, .T. ) ;
#6182=ORIENTED_EDGE ( 'NONE', *, *, #23687, .T. ) ;
#6191=ADVANCED_FACE ( 'NONE', ( #16698 ), #14635, .T. ) ;
#6244=DIRECTION ( 'NONE',  ( 0.000000000000000000, 0.000000000000000000, -1.000000000000000000 ) ) ;
#6262=ORIENTED_EDGE ( 'NONE', *, *, #19344, .F. ) ;
#6272=VECTOR ( 'NONE', #5023, 39.37007874015748143 ) ;
#6304=ORIENTED_EDGE ( 'NONE', *, *, #20311, .F. ) ;
#6316=DIRECTION ( 'NONE',  ( -0.000000000000000000, -1.000000000000000000, -0.000000000000000000 ) ) ;
#6353=AXIS2_PLACEMENT_3D ( 'NONE', #15638, #13934, #6602 ) ;
#6355=DIRECTION ( 'NONE',  ( 0.000000000000000000, 0.000000000000000000, -1.000000000000000000 ) ) ;
#6369=TOROIDAL_SURFACE ( 'NONE', #23096, 0.2510000000000000009, 0.0009999999999999896125 ) ;
#6398=ORIENTED_EDGE ( 'NONE', *, *, #6916, .T. ) ;
#6408=AXIS2_PLACEMENT_3D ( 'NONE', #14899, #11000, #20143 ) ;
#6439=EDGE_LOOP ( 'NONE', ( #8671, #24112 ) ) ;
#6471=DIRECTION ( 'NONE',  ( 0.000000000000000000, 0.000000000000000000, 1.000000000000000000 ) ) ;
#6485=ORIENTED_EDGE ( 'NONE', *, *, #11537, .F. ) ;
#6490=AXIS2_PLACEMENT_3D ( 'NONE', #14384, #12938, #21811 ) ;
#6525=CARTESIAN_POINT ( 'NONE',  ( 0.000000000000000000, 0.4997679491924311157, -0.3125000000000001665 ) ) ;
#6540=EDGE_CURVE ( 'NONE', #22476, #6959, #2997, .T. ) ;
#6589=DIRECTION ( 'NONE',  ( 0.000000000000000000, -0.000000000000000000, 1.000000000000000000 ) ) ;
#6602=DIRECTION ( 'NONE',  ( 0.000000000000000000, 0.000000000000000000, 1.000000000000000000 ) ) ;
#6615=CARTESIAN_POINT ( 'NONE',  ( 2.781172880863639385E-17, 6.000000000000000888, 0.2041999999999999926 ) ) ;
#6636=TOROIDAL_SURFACE ( 'NONE', #18702, 0.2510000000000000009, 0.001000000000000037101 ) ;
#6708=PLANE ( 'NONE',  #19110 ) ;
#6718=ORIENTED_EDGE ( 'NONE', *, *, #19005, .F. ) ;
#6730=EDGE_LOOP ( 'NONE', ( #19431, #13130, #18423, #21553 ) ) ;
#6848=CARTESIAN_POINT ( 'NONE',  ( 0.000000000000000000, 5.501232050807569607, 0.000000000000000000 ) ) ;
#6905=CARTESIAN_POINT ( 'NONE',  ( 0.000000000000000000, 5.501232050807569607, 0.000000000000000000 ) ) ;
#6916=EDGE_CURVE ( 'NONE', #22476, #13713, #13592, .T. ) ;
#6945=ADVANCED_FACE ( 'NONE', ( #18321 ), #22332, .T. ) ;
#6959=VERTEX_POINT ( 'NONE', #21678 ) ;
#6994=DIRECTION ( 'NONE',  ( 0.000000000000000000, -0.000000000000000000, 1.000000000000000000 ) ) ;
#7001=ORIENTED_EDGE ( 'NONE', *, *, #22714, .T. ) ;
#7006=PRODUCT ( 'Aloris-BXA-Handle-Rod', 'Aloris-BXA-Handle-Rod', '', ( #21995 ) ) ;
#7016=AXIS2_PLACEMENT_3D ( 'NONE', #5149, #14915, #3204 ) ;
#7091=DIRECTION ( 'NONE',  ( 0.000000000000000000, 0.000000000000000000, 1.000000000000000000 ) ) ;
#7135=CARTESIAN_POINT ( 'NONE',  ( 0.000000000000000000, 0.4202679491924311561, 0.000000000000000000 ) ) ;
#7173=FACE_OUTER_BOUND ( 'NONE', #15300, .T. ) ;
#7189=LINE ( 'NONE', #10854, #8368 ) ;
#7221=ADVANCED_FACE ( 'NONE', ( #10328 ), #21863, .F. ) ;
#7230=AXIS2_PLACEMENT_3D ( 'NONE', #16285, #9325, #21766 ) ;
#7335=DIRECTION ( 'NONE',  ( -0.000000000000000000, 1.000000000000000000, -0.000000000000000000 ) ) ;
#7376=FACE_OUTER_BOUND ( 'NONE', #18987, .T. ) ;
#7378=EDGE_LOOP ( 'NONE', ( #23948, #5913, #3011, #4652 ) ) ;
#7429=AXIS2_PLACEMENT_3D ( 'NONE', #8023, #22900, #11952 ) ;
#7438=ORIENTED_EDGE ( 'NONE', *, *, #3928, .F. ) ;
#7461=FACE_OUTER_BOUND ( 'NONE', #7930, .T. ) ;
#7528=DIRECTION ( 'NONE',  ( -0.000000000000000000, 1.000000000000000000, -0.000000000000000000 ) ) ;
#7555=CARTESIAN_POINT ( 'NONE',  ( 0.000000000000000000, 0.000000000000000000, 0.2500000000000000000 ) ) ;
#7556=DIRECTION ( 'NONE',  ( 0.000000000000000000, 0.000000000000000000, -1.000000000000000000 ) ) ;
#7570=AXIS2_PLACEMENT_3D ( 'NONE', #8266, #11827, #11589 ) ;
#7581=DIRECTION ( 'NONE',  ( -1.224646799147350495E-16, 0.000000000000000000, -1.000000000000000000 ) ) ;
#7582=DIRECTION ( 'NONE',  ( 0.000000000000000000, 0.000000000000000000, -1.000000000000000000 ) ) ;
#7641=DIRECTION ( 'NONE',  ( 0.000000000000000000, -0.8660254037843519992, -0.5000000000001502132 ) ) ;
#7682=FACE_OUTER_BOUND ( 'NONE', #5043, .T. ) ;
#7737=DIRECTION ( 'NONE',  ( -0.000000000000000000, 1.000000000000000000, -0.000000000000000000 ) ) ;
#7744=CIRCLE ( 'NONE', #14355, 0.2500000000000000000 ) ;
#7775=FACE_OUTER_BOUND ( 'NONE', #790, .T. ) ;
#7800=ADVANCED_FACE ( 'NONE', ( #7775, #14870 ), #17488, .F. ) ;
#7814=CARTESIAN_POINT ( 'NONE',  ( 0.000000000000000000, 6.000000000000000888, 0.000000000000000000 ) ) ;
#7890=ORIENTED_EDGE ( 'NONE', *, *, #23902, .F. ) ;
#7926=AXIS2_PLACEMENT_3D ( 'NONE', #9904, #747, #6355 ) ;
#7930=EDGE_LOOP ( 'NONE', ( #15727, #6718 ) ) ;
#7962=ORIENTED_EDGE ( 'NONE', *, *, #19287, .F. ) ;
#7972=DIRECTION ( 'NONE',  ( -0.000000000000000000, -1.000000000000000000, -0.000000000000000000 ) ) ;
#8023=CARTESIAN_POINT ( 'NONE',  ( 3.073863465859856523E-17, 5.579732050807569621, 0.2510000000000000009 ) ) ;
#8074=DIRECTION ( 'NONE',  ( -0.000000000000000000, 1.000000000000000000, -0.000000000000000000 ) ) ;
#8085=VERTEX_POINT ( 'NONE', #8696 ) ;
#8099=ORIENTED_EDGE ( 'NONE', *, *, #19005, .T. ) ;
#8122=ADVANCED_FACE ( 'NONE', ( #10906 ), #12870, .T. ) ;
#8175=DIRECTION ( 'NONE',  ( 1.000000000000000000, 0.000000000000000000, 1.224646799147353207E-16 ) ) ;
#8232=CARTESIAN_POINT ( 'NONE',  ( 0.000000000000000000, 0.4199999999999998734, 0.000000000000000000 ) ) ;
#8242=FACE_OUTER_BOUND ( 'NONE', #947, .T. ) ;
#8245=ADVANCED_BREP_SHAPE_REPRESENTATION ( '', ( #8780, #9127 ), #14988 ) ;
#8266=CARTESIAN_POINT ( 'NONE',  ( 0.000000000000000000, 6.000000000000000888, 0.000000000000000000 ) ) ;
#8298=DIRECTION ( 'NONE',  ( -1.000000000000000000, 0.000000000000000000, 0.000000000000000000 ) ) ;
#8368=VECTOR ( 'NONE', #11090, 39.37007874015748854 ) ;
#8392=EDGE_CURVE ( 'NONE', #2709, #14964, #22179, .T. ) ;
#8408=TOROIDAL_SURFACE ( 'NONE', #22047, 0.2510000000000000009, 0.001000000000000038835 ) ;
#8558=( NAMED_UNIT ( * ) PLANE_ANGLE_UNIT ( ) SI_UNIT ( $, .RADIAN. ) );
#8590=ORIENTED_EDGE ( 'NONE', *, *, #11416, .F. ) ;
#8671=ORIENTED_EDGE ( 'NONE', *, *, #3467, .F. ) ;
#8696=CARTESIAN_POINT ( 'NONE',  ( 3.073863465859856523E-17, 0.4997679491924311157, -0.2510000000000000009 ) ) ;
#8706=DIRECTION ( 'NONE',  ( -0.000000000000000000, -1.000000000000000000, -0.000000000000000000 ) ) ;
#8716=DIRECTION ( 'NONE',  ( -0.000000000000000000, 1.000000000000000000, -0.000000000000000000 ) ) ;
#8780=MANIFOLD_SOLID_BREP ( '1/2-13 Machine Threads Stud2', #15051 ) ;
#8798=AXIS2_PLACEMENT_3D ( 'NONE', #17251, #7972, #16884 ) ;
#8851=DIRECTION ( 'NONE',  ( 0.000000000000000000, 1.000000000000000000, 0.000000000000000000 ) ) ;
#8881=EDGE_CURVE ( 'NONE', #1686, #2709, #20466, .T. ) ;
#8911=VECTOR ( 'NONE', #16044, 39.37007874015748143 ) ;
#8950=ORIENTED_EDGE ( 'NONE', *, *, #11311, .T. ) ;
#8953=ORIENTED_EDGE ( 'NONE', *, *, #15132, .F. ) ;
#8988=ADVANCED_FACE ( 'NONE', ( #5469 ), #22945, .F. ) ;
#9037=VERTEX_POINT ( 'NONE', #460 ) ;
#9127=AXIS2_PLACEMENT_3D ( 'NONE', #15878, #23181, #23294 ) ;
#9139=CARTESIAN_POINT ( 'NONE',  ( 0.000000000000000000, 0.4199999999999998734, 0.2500000000000000555 ) ) ;
#9174=CARTESIAN_POINT ( 'NONE',  ( 0.000000000000000000, 0.000000000000000000, 0.000000000000000000 ) ) ;
#9295=CARTESIAN_POINT ( 'NONE',  ( 0.000000000000000000, 5.500232050807569273, -0.2510000000000000009 ) ) ;
#9306=DIRECTION ( 'NONE',  ( -0.000000000000000000, 1.000000000000000000, -0.000000000000000000 ) ) ;
#9313=EDGE_CURVE ( 'NONE', #11401, #1686, #15196, .T. ) ;
#9325=DIRECTION ( 'NONE',  ( -0.000000000000000000, -1.000000000000000000, -0.000000000000000000 ) ) ;
#9330=VECTOR ( 'NONE', #10968, 39.37007874015748143 ) ;
#9355=VERTEX_POINT ( 'NONE', #21306 ) ;
#9571=DIRECTION ( 'NONE',  ( 0.000000000000000000, 0.000000000000000000, 1.000000000000000000 ) ) ;
#9575=DIRECTION ( 'NONE',  ( 0.000000000000000000, 1.000000000000000000, 0.000000000000000000 ) ) ;
#9607=DIRECTION ( 'NONE',  ( -0.000000000000000000, 1.000000000000000000, -0.000000000000000000 ) ) ;
#9660=DIRECTION ( 'NONE',  ( -0.000000000000000000, -1.000000000000000000, -0.000000000000000000 ) ) ;
#9673=CARTESIAN_POINT ( 'NONE',  ( 3.063257713472607067E-17, 0.4197679491924312112, 0.2501339745962155581 ) ) ;
#9682=VERTEX_POINT ( 'NONE', #310 ) ;
#9747=CARTESIAN_POINT ( 'NONE',  ( 3.827021247335478926E-17, 6.000000000000000888, 0.3125000000000000555 ) ) ;
#9768=AXIS2_PLACEMENT_3D ( 'NONE', #14910, #139, #7582 ) ;
#9779=CARTESIAN_POINT ( 'NONE',  ( 0.000000000000000000, 0.000000000000000000, 0.000000000000000000 ) ) ;
#9787=ADVANCED_FACE ( 'NONE', ( #18 ), #11700, .F. ) ;
#9808=ORIENTED_EDGE ( 'NONE', *, *, #1859, .F. ) ;
#9880=AXIS2_PLACEMENT_3D ( 'NONE', #9779, #622, #10025 ) ;
#9895=AXIS2_PLACEMENT_3D ( 'NONE', #2586, #8175, #19159 ) ;
#9904=CARTESIAN_POINT ( 'NONE',  ( 0.000000000000000000, 5.500232050807569273, 0.000000000000000000 ) ) ;
#9916=CONICAL_SURFACE ( 'NONE', #7570, 0.2041999999999999926, 0.7853981633974621568 ) ;
#9986=DESIGN_CONTEXT ( 'detailed design', #2977, 'design' ) ;
#9987=AXIS2_PLACEMENT_3D ( 'NONE', #2015, #11650, #535 ) ;
#10025=DIRECTION ( 'NONE',  ( 0.000000000000000000, 0.000000000000000000, 1.000000000000000000 ) ) ;
#10078=ORIENTED_EDGE ( 'NONE', *, *, #6162, .T. ) ;
#10104=ORIENTED_EDGE ( 'NONE', *, *, #18001, .F. ) ;
#10119=FACE_OUTER_BOUND ( 'NONE', #4418, .T. ) ;
#10171=VECTOR ( 'NONE', #6316, 39.37007874015748143 ) ;
#10186=DIRECTION ( 'NONE',  ( 0.000000000000000000, 0.000000000000000000, 1.000000000000000000 ) ) ;
#10193=ORIENTED_EDGE ( 'NONE', *, *, #9313, .F. ) ;
#10215=CARTESIAN_POINT ( 'NONE',  ( 0.000000000000000000, 5.580000000000000959, 0.000000000000000000 ) ) ;
#10264=FACE_OUTER_BOUND ( 'NONE', #17497, .T. ) ;
#10301=CARTESIAN_POINT ( 'NONE',  ( 0.000000000000000000, 0.4202679491924311561, 0.000000000000000000 ) ) ;
#10328=FACE_OUTER_BOUND ( 'NONE', #6439, .T. ) ;
#10341=DIRECTION ( 'NONE',  ( -0.000000000000000000, 1.000000000000000000, -0.000000000000000000 ) ) ;
#10416=CARTESIAN_POINT ( 'NONE',  ( 3.061616997868383018E-17, 0.04579999999999925103, -0.2500000000000000000 ) ) ;
#10419=DIRECTION ( 'NONE',  ( -0.000000000000000000, -1.000000000000000000, -0.000000000000000000 ) ) ;
#10447=CARTESIAN_POINT ( 'NONE',  ( 3.061616997868383018E-17, 6.000000000000000888, 0.2500000000000000000 ) ) ;
#10474=ORIENTED_EDGE ( 'NONE', *, *, #22139, .T. ) ;
#10530=LINE ( 'NONE', #2962, #6272 ) ;
#10554=AXIS2_PLACEMENT_3D ( 'NONE', #22033, #20213, #21551 ) ;
#10555=ORIENTED_EDGE ( 'NONE', *, *, #14503, .F. ) ;
#10568=CARTESIAN_POINT ( 'NONE',  ( 0.000000000000000000, 5.579732050807569621, 0.000000000000000000 ) ) ;
#10644=CARTESIAN_POINT ( 'NONE',  ( 0.000000000000000000, 6.000000000000000888, -0.2499999999999999722 ) ) ;
#10658=CARTESIAN_POINT ( 'NONE',  ( 0.000000000000000000, 5.580000000000000959, 0.000000000000000000 ) ) ;
#10669=ADVANCED_FACE ( 'NONE', ( #7461, #3925 ), #22456, .F. ) ;
#10718=DIRECTION ( 'NONE',  ( 8.659560562355053653E-17, -0.7071067811865376918, 0.7071067811865573427 ) ) ;
#10789=DIRECTION ( 'NONE',  ( 0.000000000000000000, 0.000000000000000000, 1.000000000000000000 ) ) ;
#10800=EDGE_LOOP ( 'NONE', ( #8953, #10193, #19808, #17288 ) ) ;
#10805=CYLINDRICAL_SURFACE ( 'NONE', #7230, 0.2500000000000000000 ) ;
#10839=DIRECTION ( 'NONE',  ( 0.000000000000000000, 0.000000000000000000, -1.000000000000000000 ) ) ;
#10848=ADVANCED_FACE ( 'NONE', ( #10264 ), #6708, .T. ) ;
#10854=CARTESIAN_POINT ( 'NONE',  ( 0.000000000000000000, 5.580000000000000959, 0.2500000000000000555 ) ) ;
#10856=CARTESIAN_POINT ( 'NONE',  ( 0.000000000000000000, 6.000000000000000888, 0.000000000000000000 ) ) ;
#10866=CARTESIAN_POINT ( 'NONE',  ( 3.061616997868383634E-17, 0.4199999999999998734, 0.2500000000000000555 ) ) ;
#10881=CARTESIAN_POINT ( 'NONE',  ( 0.000000000000000000, 0.4997679491924311157, 0.000000000000000000 ) ) ;
#10882=AXIS2_PLACEMENT_3D ( 'NONE', #21411, #17754, #6994 ) ;
#10906=FACE_OUTER_BOUND ( 'NONE', #22657, .T. ) ;
#10968=DIRECTION ( 'NONE',  ( -0.000000000000000000, -1.000000000000000000, -0.000000000000000000 ) ) ;
#10977=FACE_OUTER_BOUND ( 'NONE', #4369, .T. ) ;
#10981=CARTESIAN_POINT ( 'NONE',  ( 0.000000000000000000, 5.501232050807569607, -0.2499999999999999722 ) ) ;
#11000=DIRECTION ( 'NONE',  ( -1.000000000000000000, 0.000000000000000000, 0.000000000000000000 ) ) ;
#11005=DIRECTION ( 'NONE',  ( -0.000000000000000000, 1.000000000000000000, -0.000000000000000000 ) ) ;
#11012=DIRECTION ( 'NONE',  ( -0.000000000000000000, -1.000000000000000000, -0.000000000000000000 ) ) ;
#11021=DIRECTION ( 'NONE',  ( 0.000000000000000000, 0.7071067811865416886, 0.7071067811865531239 ) ) ;
#11058=DIRECTION ( 'NONE',  ( -0.000000000000000000, -1.000000000000000000, -0.000000000000000000 ) ) ;
#11061=CIRCLE ( 'NONE', #9895, 0.001000000000000003057 ) ;
#11083=DIRECTION ( 'NONE',  ( -0.000000000000000000, 1.000000000000000000, -0.000000000000000000 ) ) ;
#11089=AXIS2_PLACEMENT_3D ( 'NONE', #13081, #15137, #1962 ) ;
#11090=DIRECTION ( 'NONE',  ( 0.000000000000000000, 0.8660254037842882724, 0.5000000000002605693 ) ) ;
#11159=ORIENTED_EDGE ( 'NONE', *, *, #18097, .F. ) ;
#11183=CIRCLE ( 'NONE', #659, 0.3125000000000001665 ) ;
#11198=CYLINDRICAL_SURFACE ( 'NONE', #15103, 0.3125000000000000555 ) ;
#11203=CARTESIAN_POINT ( 'NONE',  ( 2.500728763858895135E-17, 6.000000000000000888, 0.2041999999999999926 ) ) ;
#11223=DIRECTION ( 'NONE',  ( -0.000000000000000000, -1.000000000000000000, -0.000000000000000000 ) ) ;
#11251=CARTESIAN_POINT ( 'NONE',  ( 3.073863465859856523E-17, 5.501232050807569607, 0.2510000000000000009 ) ) ;
#11267=DIRECTION ( 'NONE',  ( -0.000000000000000000, 1.000000000000000000, -0.000000000000000000 ) ) ;
#11287=CARTESIAN_POINT ( 'NONE',  ( 0.000000000000000000, 0.000000000000000000, 0.000000000000000000 ) ) ;
#11307=DIRECTION ( 'NONE',  ( 6.123233995739957225E-17, 0.8660254037842882724, -0.5000000000002605693 ) ) ;
#11311=EDGE_CURVE ( 'NONE', #17737, #4761, #21060, .T. ) ;
#11401=VERTEX_POINT ( 'NONE', #17138 ) ;
#11416=EDGE_CURVE ( 'NONE', #404, #12951, #22609, .T. ) ;
#11502=AXIS2_PLACEMENT_3D ( 'NONE', #12183, #10341, #1305 ) ;
#11513=AXIS2_PLACEMENT_3D ( 'NONE', #1281, #8706, #14328 ) ;
#11537=EDGE_CURVE ( 'NONE', #6959, #9037, #18340, .T. ) ;
#11575=AXIS2_PLACEMENT_3D ( 'NONE', #13062, #23756, #20480 ) ;
#11589=DIRECTION ( 'NONE',  ( 0.000000000000000000, 0.000000000000000000, -1.000000000000000000 ) ) ;
#11630=CARTESIAN_POINT ( 'NONE',  ( 2.500728763858895135E-17, 0.000000000000000000, -0.2041999999999999926 ) ) ;
#11632=ORIENTED_EDGE ( 'NONE', *, *, #17389, .F. ) ;
#11650=DIRECTION ( 'NONE',  ( -0.000000000000000000, 1.000000000000000000, -0.000000000000000000 ) ) ;
#11688=AXIS2_PLACEMENT_3D ( 'NONE', #24050, #9306, #10789 ) ;
#11700=CONICAL_SURFACE ( 'NONE', #7016, 0.2500000000000000555, 0.5235987755984723435 ) ;
#11757=FACE_OUTER_BOUND ( 'NONE', #3476, .T. ) ;
#11827=DIRECTION ( 'NONE',  ( -0.000000000000000000, -1.000000000000000000, -0.000000000000000000 ) ) ;
#11853=VECTOR ( 'NONE', #19636, 39.37007874015748143 ) ;
#11863=ORIENTED_EDGE ( 'NONE', *, *, #20996, .F. ) ;
#11939=DIRECTION ( 'NONE',  ( -0.000000000000000000, -1.000000000000000000, -0.000000000000000000 ) ) ;
#11952=DIRECTION ( 'NONE',  ( -1.224646799147350495E-16, 0.000000000000000000, -1.000000000000000000 ) ) ;
#11967=ORIENTED_EDGE ( 'NONE', *, *, #11537, .T. ) ;
#12058=ORIENTED_EDGE ( 'NONE', *, *, #12758, .T. ) ;
#12164=CYLINDRICAL_SURFACE ( 'NONE', #18927, 0.2500000000000000000 ) ;
#12183=CARTESIAN_POINT ( 'NONE',  ( 0.000000000000000000, 0.4197679491924312112, 0.000000000000000000 ) ) ;
#12188=VECTOR ( 'NONE', #11021, 39.37007874015748854 ) ;
#12210=AXIS2_PLACEMENT_3D ( 'NONE', #20133, #19890, #7091 ) ;
#12227=CARTESIAN_POINT ( 'NONE',  ( 3.061616997868383018E-17, 0.000000000000000000, -0.2500000000000000000 ) ) ;
#12238=DIRECTION ( 'NONE',  ( -0.000000000000000000, -1.000000000000000000, -0.000000000000000000 ) ) ;
#12339=CONICAL_SURFACE ( 'NONE', #2204, 0.2500000000000000555, 0.5235987755985997971 ) ;
#12359=CIRCLE ( 'NONE', #23232, 0.001000000000000037101 ) ;
#12380=EDGE_LOOP ( 'NONE', ( #997, #231, #11632, #23290 ) ) ;
#12471=EDGE_LOOP ( 'NONE', ( #18128, #20415, #8950, #21868 ) ) ;
#12488=LINE ( 'NONE', #10644, #15195 ) ;
#12525=ORIENTED_EDGE ( 'NONE', *, *, #2142, .F. ) ;
#12587=CIRCLE ( 'NONE', #6353, 0.001000000000000037101 ) ;
#12698=DIRECTION ( 'NONE',  ( 0.000000000000000000, 0.000000000000000000, -1.000000000000000000 ) ) ;
#12715=CIRCLE ( 'NONE', #19298, 0.2499999999999999722 ) ;
#12758=EDGE_CURVE ( 'NONE', #21481, #13713, #19627, .T. ) ;
#12857=CARTESIAN_POINT ( 'NONE',  ( 0.000000000000000000, 5.954200000000001936, 0.000000000000000000 ) ) ;
#12870=CYLINDRICAL_SURFACE ( 'NONE', #11688, 0.2500000000000000000 ) ;
#12911=ADVANCED_FACE ( 'NONE', ( #10977 ), #1997, .F. ) ;
#12913=ADVANCED_FACE ( 'NONE', ( #14389 ), #13264, .F. ) ;
#12938=DIRECTION ( 'NONE',  ( -0.000000000000000000, 1.000000000000000000, -0.000000000000000000 ) ) ;
#12951=VERTEX_POINT ( 'NONE', #6525 ) ;
#13016=DIRECTION ( 'NONE',  ( 0.000000000000000000, 0.000000000000000000, -1.000000000000000000 ) ) ;
#13062=CARTESIAN_POINT ( 'NONE',  ( 0.000000000000000000, 6.000000000000000888, 0.000000000000000000 ) ) ;
#13066=DIRECTION ( 'NONE',  ( -0.000000000000000000, 1.000000000000000000, -0.000000000000000000 ) ) ;
#13081=CARTESIAN_POINT ( 'NONE',  ( 0.000000000000000000, 0.000000000000000000, 0.000000000000000000 ) ) ;
#13094=ORIENTED_EDGE ( 'NONE', *, *, #13533, .T. ) ;
#13130=ORIENTED_EDGE ( 'NONE', *, *, #15111, .T. ) ;
#13154=LINE ( 'NONE', #14605, #19590 ) ;
#13174=PRODUCT_DEFINITION ( 'UNKNOWN', '', #4493, #9986 ) ;
#13250=CYLINDRICAL_SURFACE ( 'NONE', #1026, 0.2500000000000000000 ) ;
#13264=TOROIDAL_SURFACE ( 'NONE', #2728, 0.2510000000000000009, 0.001000000000000038835 ) ;
#13311=AXIS2_PLACEMENT_3D ( 'NONE', #104, #14879, #5593 ) ;
#13362=FACE_OUTER_BOUND ( 'NONE', #5282, .T. ) ;
#13369=CIRCLE ( 'NONE', #19577, 0.2500000000000000555 ) ;
#13380=DIRECTION ( 'NONE',  ( 0.000000000000000000, 0.000000000000000000, 1.000000000000000000 ) ) ;
#13382=CARTESIAN_POINT ( 'NONE',  ( 0.000000000000000000, 0.4199999999999998734, -0.2500000000000000555 ) ) ;
#13404=CIRCLE ( 'NONE', #4809, 0.001000000000000037101 ) ;
#13417=AXIS2_PLACEMENT_3D ( 'NONE', #15098, #7528, #3987 ) ;
#13439=FACE_OUTER_BOUND ( 'NONE', #15329, .T. ) ;
#13502=EDGE_LOOP ( 'NONE', ( #21106, #5360, #2271, #16623 ) ) ;
#13516=VERTEX_POINT ( 'NONE', #6615 ) ;
#13525=EDGE_CURVE ( 'NONE', #17212, #17737, #10530, .T. ) ;
#13527=EDGE_CURVE ( 'NONE', #11401, #14964, #12488, .T. ) ;
#13533=EDGE_CURVE ( 'NONE', #18846, #409, #17523, .T. ) ;
#13540=AXIS2_PLACEMENT_3D ( 'NONE', #10301, #3323, #2841 ) ;
#13592=CIRCLE ( 'NONE', #16692, 0.2500000000000000000 ) ;
#13598=EDGE_LOOP ( 'NONE', ( #1470, #16636, #10474, #21005 ) ) ;
#13708=( NAMED_UNIT ( * ) SI_UNIT ( $, .STERADIAN. ) SOLID_ANGLE_UNIT ( ) );
#13713=VERTEX_POINT ( 'NONE', #19823 ) ;
#13737=CARTESIAN_POINT ( 'NONE',  ( 0.000000000000000000, 0.4987679491924311148, 0.000000000000000000 ) ) ;
#13748=VECTOR ( 'NONE', #4727, 39.37007874015748143 ) ;
#13783=ADVANCED_FACE ( 'NONE', ( #17999 ), #21432, .F. ) ;
#13803=CARTESIAN_POINT ( 'NONE',  ( 0.000000000000000000, 6.000000000000000888, 0.000000000000000000 ) ) ;
#13820=CIRCLE ( 'NONE', #16927, 0.2510000000000000009 ) ;
#13845=VERTEX_POINT ( 'NONE', #23643 ) ;
#13934=DIRECTION ( 'NONE',  ( -1.000000000000000000, 0.000000000000000000, 0.000000000000000000 ) ) ;
#14059=ADVANCED_FACE ( 'NONE', ( #18533 ), #6636, .F. ) ;
#14094=VERTEX_POINT ( 'NONE', #1594 ) ;
#14201=CIRCLE ( 'NONE', #6408, 0.001000000000000003057 ) ;
#14209=ORIENTED_EDGE ( 'NONE', *, *, #12758, .F. ) ;
#14301=ORIENTED_EDGE ( 'NONE', *, *, #22714, .F. ) ;
#14328=DIRECTION ( 'NONE',  ( 0.000000000000000000, 0.000000000000000000, -1.000000000000000000 ) ) ;
#14337=FACE_OUTER_BOUND ( 'NONE', #7378, .T. ) ;
#14343=DIRECTION ( 'NONE',  ( -0.000000000000000000, -1.000000000000000000, -0.000000000000000000 ) ) ;
#14355=AXIS2_PLACEMENT_3D ( 'NONE', #19038, #16962, #20620 ) ;
#14384=CARTESIAN_POINT ( 'NONE',  ( 0.000000000000000000, 0.4197679491924312112, 0.000000000000000000 ) ) ;
#14389=FACE_OUTER_BOUND ( 'NONE', #10800, .T. ) ;
#14503=EDGE_CURVE ( 'NONE', #9355, #20185, #406, .T. ) ;
#14511=DIRECTION ( 'NONE',  ( 0.000000000000000000, 0.000000000000000000, -1.000000000000000000 ) ) ;
#14565=CIRCLE ( 'NONE', #18064, 0.2500000000000000000 ) ;
#14604=PRODUCT_DEFINITION_SHAPE ( 'NONE', 'NONE',  #13174 ) ;
#14605=CARTESIAN_POINT ( 'NONE',  ( 3.061616997868383634E-17, 5.580000000000000959, -0.2500000000000000555 ) ) ;
#14616=DIRECTION ( 'NONE',  ( -0.000000000000000000, -1.000000000000000000, -0.000000000000000000 ) ) ;
#14632=DIRECTION ( 'NONE',  ( -0.000000000000000000, -1.000000000000000000, -0.000000000000000000 ) ) ;
#14635=CYLINDRICAL_SURFACE ( 'NONE', #20589, 0.2500000000000000000 ) ;
#14695=ORIENTED_EDGE ( 'NONE', *, *, #21858, .F. ) ;
#14697=ADVANCED_FACE ( 'NONE', ( #15287 ), #3930, .T. ) ;
#14710=ADVANCED_FACE ( 'NONE', ( #11757 ), #19105, .F. ) ;
#14724=AXIS2_PLACEMENT_3D ( 'NONE', #6905, #14343, #21776 ) ;
#14769=ORIENTED_EDGE ( 'NONE', *, *, #16335, .T. ) ;
#14810=AXIS2_PLACEMENT_3D ( 'NONE', #6848, #12238, #4537 ) ;
#14846=EDGE_LOOP ( 'NONE', ( #5779, #19283, #20308, #19901 ) ) ;
#14870=FACE_BOUND ( 'NONE', #15133, .T. ) ;
#14879=DIRECTION ( 'NONE',  ( -0.000000000000000000, -1.000000000000000000, -0.000000000000000000 ) ) ;
#14893=CARTESIAN_POINT ( 'NONE',  ( 0.000000000000000000, 0.4202679491924311006, 0.000000000000000000 ) ) ;
#14899=CARTESIAN_POINT ( 'NONE',  ( 0.000000000000000000, 0.4987679491924311148, 0.2510000000000000009 ) ) ;
#14909=DIRECTION ( 'NONE',  ( 1.000000000000000000, 0.000000000000000000, -1.224646799147353207E-16 ) ) ;
#14910=CARTESIAN_POINT ( 'NONE',  ( 0.2510000000000000009, 5.500232050807569273, 0.000000000000000000 ) ) ;
#14914=DIRECTION ( 'NONE',  ( 0.000000000000000000, 0.000000000000000000, -1.000000000000000000 ) ) ;
#14915=DIRECTION ( 'NONE',  ( 0.000000000000000000, -1.000000000000000000, 0.000000000000000000 ) ) ;
#14929=AXIS2_PLACEMENT_3D ( 'NONE', #6143, #9575, #6022 ) ;
#14963=VECTOR ( 'NONE', #13066, 39.37007874015748143 ) ;
#14964=VERTEX_POINT ( 'NONE', #10981 ) ;
#14988=( GEOMETRIC_REPRESENTATION_CONTEXT ( 3 ) GLOBAL_UNCERTAINTY_ASSIGNED_CONTEXT ( ( #704 ) ) GLOBAL_UNIT_ASSIGNED_CONTEXT ( ( #17589, #8558, #13708 ) ) REPRESENTATION_CONTEXT ( 'NONE', 'WORKASPACE' ) );
#15032=VECTOR ( 'NONE', #7641, 39.37007874015748854 ) ;
#15034=DIRECTION ( 'NONE',  ( 0.000000000000000000, 0.000000000000000000, -1.000000000000000000 ) ) ;
#15051=CLOSED_SHELL ( 'NONE', ( #20692, #5290, #6945, #8988, #9787, #8122, #19584, #12911, #21240, #871, #1122, #22991, #2420, #3208, #6191, #16817, #12913, #19006, #14059, #10669, #14697, #10848, #23649, #13783, #17769, #23446, #14710, #7800, #18020, #7221 ) ) ;
#15098=CARTESIAN_POINT ( 'NONE',  ( 0.000000000000000000, 0.04579999999999925103, 0.000000000000000000 ) ) ;
#15103=AXIS2_PLACEMENT_3D ( 'NONE', #22282, #14616, #10839 ) ;
#15111=EDGE_CURVE ( 'NONE', #19709, #404, #19125, .T. ) ;
#15118=ORIENTED_EDGE ( 'NONE', *, *, #3928, .T. ) ;
#15132=EDGE_CURVE ( 'NONE', #1686, #21793, #1190, .T. ) ;
#15133=EDGE_LOOP ( 'NONE', ( #1570, #14769 ) ) ;
#15137=DIRECTION ( 'NONE',  ( -0.000000000000000000, 1.000000000000000000, -0.000000000000000000 ) ) ;
#15169=DIRECTION ( 'NONE',  ( 0.000000000000000000, 0.000000000000000000, -1.000000000000000000 ) ) ;
#15172=ORIENTED_EDGE ( 'NONE', *, *, #19009, .F. ) ;
#15195=VECTOR ( 'NONE', #23666, 39.37007874015748143 ) ;
#15196=CIRCLE ( 'NONE', #778, 0.2499999999999999722 ) ;
#15205=ORIENTED_EDGE ( 'NONE', *, *, #20996, .T. ) ;
#15227=EDGE_LOOP ( 'NONE', ( #13094, #2746 ) ) ;
#15287=FACE_OUTER_BOUND ( 'NONE', #15316, .T. ) ;
#15300=EDGE_LOOP ( 'NONE', ( #4158, #8099, #3898, #21089 ) ) ;
#15310=CONICAL_SURFACE ( 'NONE', #14929, 0.2500000000000000555, 0.5235987755985997971 ) ;
#15316=EDGE_LOOP ( 'NONE', ( #18780, #1166, #12058, #22600 ) ) ;
#15321=CONICAL_SURFACE ( 'NONE', #9880, 0.2041999999999999926, 0.7853981633974563836 ) ;
#15329=EDGE_LOOP ( 'NONE', ( #4549, #2076, #7438, #20134 ) ) ;
#15344=AXIS2_PLACEMENT_3D ( 'NONE', #13803, #21112, #21472 ) ;
#15397=AXIS2_PLACEMENT_3D ( 'NONE', #3642, #14632, #23998 ) ;
#15410=DIRECTION ( 'NONE',  ( -0.000000000000000000, -1.000000000000000000, -0.000000000000000000 ) ) ;
#15440=EDGE_CURVE ( 'NONE', #9682, #2851, #3326, .T. ) ;
#15444=CIRCLE ( 'NONE', #6490, 0.2501339745962155581 ) ;
#15478=ORIENTED_EDGE ( 'NONE', *, *, #18257, .T. ) ;
#15514=VECTOR ( 'NONE', #10718, 39.37007874015748143 ) ;
#15564=DIRECTION ( 'NONE',  ( 0.000000000000000000, 0.000000000000000000, -1.000000000000000000 ) ) ;
#15572=CARTESIAN_POINT ( 'NONE',  ( 0.000000000000000000, 0.4997679491924311157, 0.000000000000000000 ) ) ;
#15586=CARTESIAN_POINT ( 'NONE',  ( 3.061616997868383018E-17, 5.954200000000001936, 0.2500000000000000000 ) ) ;
#15638=CARTESIAN_POINT ( 'NONE',  ( 0.000000000000000000, 5.579732050807569621, -0.2510000000000000009 ) ) ;
#15727=ORIENTED_EDGE ( 'NONE', *, *, #23851, .F. ) ;
#15758=EDGE_CURVE ( 'NONE', #23209, #12951, #4966, .T. ) ;
#15814=VERTEX_POINT ( 'NONE', #19727 ) ;
#15841=EDGE_LOOP ( 'NONE', ( #20532, #5371, #15205, #10555 ) ) ;
#15878=CARTESIAN_POINT ( 'NONE',  ( 0.000000000000000000, 0.000000000000000000, 0.000000000000000000 ) ) ;
#15888=DIRECTION ( 'NONE',  ( 0.000000000000000000, 0.000000000000000000, -1.000000000000000000 ) ) ;
#16009=AXIS2_PLACEMENT_3D ( 'NONE', #22967, #21270, #10186 ) ;
#16033=EDGE_CURVE ( 'NONE', #21793, #13845, #22292, .T. ) ;
#16044=DIRECTION ( 'NONE',  ( -0.000000000000000000, -1.000000000000000000, -0.000000000000000000 ) ) ;
#16123=VECTOR ( 'NONE', #1233, 39.37007874015748854 ) ;
#16137=CARTESIAN_POINT ( 'NONE',  ( 0.000000000000000000, 6.000000000000000888, 0.000000000000000000 ) ) ;
#16138=CARTESIAN_POINT ( 'NONE',  ( 0.000000000000000000, 0.04579999999999925103, 0.2500000000000000000 ) ) ;
#16141=CIRCLE ( 'NONE', #13417, 0.2500000000000000000 ) ;
#16277=CARTESIAN_POINT ( 'NONE',  ( 0.000000000000000000, 5.580232050807569344, 0.2501339745962155581 ) ) ;
#16285=CARTESIAN_POINT ( 'NONE',  ( 0.000000000000000000, 6.000000000000000888, 0.000000000000000000 ) ) ;
#16316=CARTESIAN_POINT ( 'NONE',  ( 0.000000000000000000, 0.4202679491924311006, 0.2510000000000000009 ) ) ;
#16335=EDGE_CURVE ( 'NONE', #8085, #14094, #21129, .T. ) ;
#16377=CARTESIAN_POINT ( 'NONE',  ( 3.062437355670495659E-17, 5.579732050807569621, 0.2499999999999999722 ) ) ;
#16405=DIRECTION ( 'NONE',  ( -0.000000000000000000, 1.000000000000000000, -0.000000000000000000 ) ) ;
#16442=CARTESIAN_POINT ( 'NONE',  ( 0.000000000000000000, 5.580232050807569344, 0.000000000000000000 ) ) ;
#16603=FACE_OUTER_BOUND ( 'NONE', #12380, .T. ) ;
#16623=ORIENTED_EDGE ( 'NONE', *, *, #19414, .F. ) ;
#16636=ORIENTED_EDGE ( 'NONE', *, *, #16780, .T. ) ;
#16671=CIRCLE ( 'NONE', #6150, 0.2499999999999999722 ) ;
#16692=AXIS2_PLACEMENT_3D ( 'NONE', #12857, #11012, #15034 ) ;
#16698=FACE_OUTER_BOUND ( 'NONE', #2492, .T. ) ;
#16780=EDGE_CURVE ( 'NONE', #9037, #6959, #13369, .T. ) ;
#16817=ADVANCED_FACE ( 'NONE', ( #22735 ), #15310, .F. ) ;
#16830=CARTESIAN_POINT ( 'NONE',  ( 0.000000000000000000, 5.954200000000001936, 0.000000000000000000 ) ) ;
#16884=DIRECTION ( 'NONE',  ( 0.000000000000000000, 0.000000000000000000, -1.000000000000000000 ) ) ;
#16921=DIRECTION ( 'NONE',  ( -0.000000000000000000, 1.000000000000000000, 0.000000000000000000 ) ) ;
#16927=AXIS2_PLACEMENT_3D ( 'NONE', #10881, #7335, #23776 ) ;
#16931=AXIS2_PLACEMENT_3D ( 'NONE', #7814, #4510, #4272 ) ;
#16955=SHAPE_REPRESENTATION ( 'Aloris-BXA-Handle-Rod', ( #9127 ), #14988 ) ;
#16962=DIRECTION ( 'NONE',  ( -0.000000000000000000, 1.000000000000000000, -0.000000000000000000 ) ) ;
#17138=CARTESIAN_POINT ( 'NONE',  ( 0.000000000000000000, 5.579732050807569621, -0.2499999999999999722 ) ) ;
#17143=EDGE_LOOP ( 'NONE', ( #24031, #19486, #18794, #5319 ) ) ;
#17212=VERTEX_POINT ( 'NONE', #395 ) ;
#17214=DIRECTION ( 'NONE',  ( -0.000000000000000000, -1.000000000000000000, -0.000000000000000000 ) ) ;
#17236=SHAPE_DEFINITION_REPRESENTATION ( #14604, #16955 ) ;
#17249=ORIENTED_EDGE ( 'NONE', *, *, #4831, .T. ) ;
#17251=CARTESIAN_POINT ( 'NONE',  ( 0.000000000000000000, 5.500232050807569273, 0.000000000000000000 ) ) ;
#17288=ORIENTED_EDGE ( 'NONE', *, *, #20468, .T. ) ;
#17348=( LENGTH_UNIT ( ) NAMED_UNIT ( * ) SI_UNIT ( $, .METRE. ) );
#17365=EDGE_CURVE ( 'NONE', #11401, #13845, #12587, .T. ) ;
#17389=EDGE_CURVE ( 'NONE', #2851, #5871, #20750, .T. ) ;
#17449=LINE ( 'NONE', #743, #21305 ) ;
#17473=CARTESIAN_POINT ( 'NONE',  ( 0.000000000000000000, 6.000000000000000888, 0.000000000000000000 ) ) ;
#17488=PLANE ( 'NONE',  #2693 ) ;
#17497=EDGE_LOOP ( 'NONE', ( #19932, #1991 ) ) ;
#17523=CIRCLE ( 'NONE', #5098, 0.2510000000000000009 ) ;
#17558=AXIS2_PLACEMENT_3D ( 'NONE', #17473, #15410, #15169 ) ;
#17589=( CONVERSION_BASED_UNIT ( 'INCH', #21603 ) LENGTH_UNIT ( ) NAMED_UNIT ( #19586 ) );
#17657=CARTESIAN_POINT ( 'NONE',  ( 3.061616997868382402E-17, 5.501232050807569607, 0.2499999999999999722 ) ) ;
#17686=CARTESIAN_POINT ( 'NONE',  ( 3.073863465859856523E-17, 0.4987679491924311148, -0.2510000000000000009 ) ) ;
#17694=FACE_OUTER_BOUND ( 'NONE', #14846, .T. ) ;
#17737=VERTEX_POINT ( 'NONE', #18778 ) ;
#17754=DIRECTION ( 'NONE',  ( 0.000000000000000000, 1.000000000000000000, 0.000000000000000000 ) ) ;
#17769=ADVANCED_FACE ( 'NONE', ( #7682 ), #6369, .F. ) ;
#17830=CIRCLE ( 'NONE', #14724, 0.2499999999999999722 ) ;
#17930=DIRECTION ( 'NONE',  ( -0.000000000000000000, 1.000000000000000000, -0.000000000000000000 ) ) ;
#17997=ORIENTED_EDGE ( 'NONE', *, *, #8392, .T. ) ;
#17999=FACE_OUTER_BOUND ( 'NONE', #1433, .T. ) ;
#18001=EDGE_CURVE ( 'NONE', #2257, #15814, #1306, .T. ) ;
#18020=ADVANCED_FACE ( 'NONE', ( #22811 ), #15321, .T. ) ;
#18051=AXIS2_PLACEMENT_3D ( 'NONE', #17686, #22691, #2692 ) ;
#18064=AXIS2_PLACEMENT_3D ( 'NONE', #16830, #11223, #3899 ) ;
#18097=EDGE_CURVE ( 'NONE', #8085, #17737, #2484, .T. ) ;
#18103=CIRCLE ( 'NONE', #11502, 0.2501339745962155581 ) ;
#18128=ORIENTED_EDGE ( 'NONE', *, *, #16335, .F. ) ;
#18257=EDGE_CURVE ( 'NONE', #9037, #13845, #13154, .T. ) ;
#18284=DIRECTION ( 'NONE',  ( -0.000000000000000000, -1.000000000000000000, -0.000000000000000000 ) ) ;
#18301=EDGE_CURVE ( 'NONE', #2851, #2257, #5326, .T. ) ;
#18321=FACE_OUTER_BOUND ( 'NONE', #13502, .T. ) ;
#18340=CIRCLE ( 'NONE', #19891, 0.2500000000000000555 ) ;
#18423=ORIENTED_EDGE ( 'NONE', *, *, #11416, .T. ) ;
#18433=DIRECTION ( 'NONE',  ( 0.000000000000000000, 0.000000000000000000, 1.000000000000000000 ) ) ;
#18486=DIRECTION ( 'NONE',  ( 0.000000000000000000, 0.000000000000000000, -1.000000000000000000 ) ) ;
#18513=DIRECTION ( 'NONE',  ( 0.000000000000000000, 0.000000000000000000, 1.000000000000000000 ) ) ;
#18533=FACE_OUTER_BOUND ( 'NONE', #563, .T. ) ;
#18569=CARTESIAN_POINT ( 'NONE',  ( 0.000000000000000000, 0.000000000000000000, 0.2041999999999999926 ) ) ;
#18589=CIRCLE ( 'NONE', #13540, 0.2499999999999999722 ) ;
#18609=ORIENTED_EDGE ( 'NONE', *, *, #22139, .F. ) ;
#18632=LINE ( 'NONE', #11203, #15514 ) ;
#18642=DIRECTION ( 'NONE',  ( -0.000000000000000000, -1.000000000000000000, -0.000000000000000000 ) ) ;
#18660=ORIENTED_EDGE ( 'NONE', *, *, #19008, .F. ) ;
#18702=AXIS2_PLACEMENT_3D ( 'NONE', #3536, #1823, #7556 ) ;
#18740=VECTOR ( 'NONE', #2690, 39.37007874015748143 ) ;
#18749=DIRECTION ( 'NONE',  ( -0.000000000000000000, -1.000000000000000000, -0.000000000000000000 ) ) ;
#18778=CARTESIAN_POINT ( 'NONE',  ( 3.061616997868383018E-17, 0.4987679491924311148, -0.2500000000000000000 ) ) ;
#18780=ORIENTED_EDGE ( 'NONE', *, *, #4831, .F. ) ;
#18794=ORIENTED_EDGE ( 'NONE', *, *, #16033, .T. ) ;
#18817=EDGE_CURVE ( 'NONE', #21481, #13516, #22733, .T. ) ;
#18846=VERTEX_POINT ( 'NONE', #9295 ) ;
#18872=DIRECTION ( 'NONE',  ( -0.000000000000000000, 1.000000000000000000, -0.000000000000000000 ) ) ;
#18927=AXIS2_PLACEMENT_3D ( 'NONE', #19945, #8716, #23581 ) ;
#18980=LINE ( 'NONE', #13382, #15032 ) ;
#18987=EDGE_LOOP ( 'NONE', ( #5945, #20508, #19203, #9808 ) ) ;
#19005=EDGE_CURVE ( 'NONE', #19709, #23209, #19232, .T. ) ;
#19006=ADVANCED_FACE ( 'NONE', ( #17694 ), #22934, .T. ) ;
#19008=EDGE_CURVE ( 'NONE', #18846, #14964, #13404, .T. ) ;
#19009=EDGE_CURVE ( 'NONE', #17212, #20917, #11061, .T. ) ;
#19038=CARTESIAN_POINT ( 'NONE',  ( 0.000000000000000000, 0.4987679491924311148, 0.000000000000000000 ) ) ;
#19105=TOROIDAL_SURFACE ( 'NONE', #17, 0.2510000000000000009, 0.0009999999999999859262 ) ;
#19110=AXIS2_PLACEMENT_3D ( 'NONE', #2932, #2462, #6589 ) ;
#19125=LINE ( 'NONE', #9747, #10171 ) ;
#19137=DIRECTION ( 'NONE',  ( 0.000000000000000000, 0.000000000000000000, 1.000000000000000000 ) ) ;
#19159=DIRECTION ( 'NONE',  ( 1.224646799147354193E-16, 0.000000000000000000, -1.000000000000000000 ) ) ;
#19171=EDGE_CURVE ( 'NONE', #2257, #20185, #23762, .T. ) ;
#19179=CARTESIAN_POINT ( 'NONE',  ( 0.000000000000000000, 0.4987679491924311148, 0.000000000000000000 ) ) ;
#19203=ORIENTED_EDGE ( 'NONE', *, *, #16780, .F. ) ;
#19232=CIRCLE ( 'NONE', #7926, 0.3125000000000001665 ) ;
#19265=CARTESIAN_POINT ( 'NONE',  ( 3.073863465859856523E-17, 5.500232050807569273, 0.2510000000000000009 ) ) ;
#19279=CARTESIAN_POINT ( 'NONE',  ( 0.000000000000000000, 5.501232050807569607, -0.2510000000000000009 ) ) ;
#19283=ORIENTED_EDGE ( 'NONE', *, *, #23423, .T. ) ;
#19287=EDGE_CURVE ( 'NONE', #5871, #15814, #22067, .T. ) ;
#19298=AXIS2_PLACEMENT_3D ( 'NONE', #10568, #21523, #4813 ) ;
#19344=EDGE_CURVE ( 'NONE', #13713, #22476, #14565, .T. ) ;
#19382=ORIENTED_EDGE ( 'NONE', *, *, #19752, .T. ) ;
#19413=CARTESIAN_POINT ( 'NONE',  ( 0.000000000000000000, 5.580232050807569344, 0.000000000000000000 ) ) ;
#19414=EDGE_CURVE ( 'NONE', #9355, #4761, #113, .T. ) ;
#19431=ORIENTED_EDGE ( 'NONE', *, *, #23851, .T. ) ;
#19486=ORIENTED_EDGE ( 'NONE', *, *, #15132, .T. ) ;
#19577=AXIS2_PLACEMENT_3D ( 'NONE', #23707, #5433, #13016 ) ;
#19584=ADVANCED_FACE ( 'NONE', ( #10119 ), #9916, .T. ) ;
#19586=DIMENSIONAL_EXPONENTS ( 1.000000000000000000, 0.000000000000000000, 0.000000000000000000, 0.000000000000000000, 0.000000000000000000, 0.000000000000000000, 0.000000000000000000 ) ;
#19590=VECTOR ( 'NONE', #11307, 39.37007874015748854 ) ;
#19625=CIRCLE ( 'NONE', #20038, 0.2501339745962155581 ) ;
#19626=CARTESIAN_POINT ( 'NONE',  ( 2.781172880863639385E-17, 0.000000000000000000, -0.2041999999999999926 ) ) ;
#19627=LINE ( 'NONE', #2923, #18740 ) ;
#19636=DIRECTION ( 'NONE',  ( -0.000000000000000000, 1.000000000000000000, -0.000000000000000000 ) ) ;
#19661=ORIENTED_EDGE ( 'NONE', *, *, #1859, .T. ) ;
#19709=VERTEX_POINT ( 'NONE', #2899 ) ;
#19727=CARTESIAN_POINT ( 'NONE',  ( 3.061616997868383634E-17, 0.4199999999999998734, -0.2500000000000000555 ) ) ;
#19752=EDGE_CURVE ( 'NONE', #5871, #2851, #16141, .T. ) ;
#19808=ORIENTED_EDGE ( 'NONE', *, *, #17365, .T. ) ;
#19820=AXIS2_PLACEMENT_3D ( 'NONE', #9174, #5268, #1735 ) ;
#19823=CARTESIAN_POINT ( 'NONE',  ( 0.000000000000000000, 5.954200000000001936, -0.2500000000000000000 ) ) ;
#19863=AXIS2_PLACEMENT_3D ( 'NONE', #8232, #3118, #15564 ) ;
#19879=ORIENTED_EDGE ( 'NONE', *, *, #13533, .F. ) ;
#19890=DIRECTION ( 'NONE',  ( -0.000000000000000000, 1.000000000000000000, -0.000000000000000000 ) ) ;
#19891=AXIS2_PLACEMENT_3D ( 'NONE', #10658, #23679, #23801 ) ;
#19901=ORIENTED_EDGE ( 'NONE', *, *, #8392, .F. ) ;
#19932=ORIENTED_EDGE ( 'NONE', *, *, #18817, .F. ) ;
#19945=CARTESIAN_POINT ( 'NONE',  ( 0.000000000000000000, 0.000000000000000000, 0.000000000000000000 ) ) ;
#20038=AXIS2_PLACEMENT_3D ( 'NONE', #19413, #4416, #6244 ) ;
#20133=CARTESIAN_POINT ( 'NONE',  ( 0.000000000000000000, 0.04579999999999925103, 0.000000000000000000 ) ) ;
#20134=ORIENTED_EDGE ( 'NONE', *, *, #13527, .F. ) ;
#20143=DIRECTION ( 'NONE',  ( 0.000000000000000000, 0.000000000000000000, 1.000000000000000000 ) ) ;
#20173=ORIENTED_EDGE ( 'NONE', *, *, #19008, .T. ) ;
#20185=VERTEX_POINT ( 'NONE', #9673 ) ;
#20196=EDGE_CURVE ( 'NONE', #22114, #5871, #20529, .T. ) ;
#20213=DIRECTION ( 'NONE',  ( -0.000000000000000000, 1.000000000000000000, -0.000000000000000000 ) ) ;
#20276=AXIS2_PLACEMENT_3D ( 'NONE', #16316, #22159, #1796 ) ;
#20308=ORIENTED_EDGE ( 'NONE', *, *, #13527, .T. ) ;
#20311=EDGE_CURVE ( 'NONE', #15814, #2257, #22748, .T. ) ;
#20414=DIRECTION ( 'NONE',  ( 0.000000000000000000, 0.000000000000000000, 1.000000000000000000 ) ) ;
#20415=ORIENTED_EDGE ( 'NONE', *, *, #18097, .T. ) ;
#20454=CIRCLE ( 'NONE', #11513, 0.2510000000000000009 ) ;
#20466=LINE ( 'NONE', #3517, #9330 ) ;
#20468=EDGE_CURVE ( 'NONE', #13845, #21793, #19625, .T. ) ;
#20480=DIRECTION ( 'NONE',  ( 0.000000000000000000, 0.000000000000000000, -1.000000000000000000 ) ) ;
#20508=ORIENTED_EDGE ( 'NONE', *, *, #6540, .T. ) ;
#20529=LINE ( 'NONE', #11630, #3670 ) ;
#20532=ORIENTED_EDGE ( 'NONE', *, *, #2897, .F. ) ;
#20569=AXIS2_PLACEMENT_3D ( 'NONE', #13737, #22636, #13380 ) ;
#20578=DIRECTION ( 'NONE',  ( 0.000000000000000000, 0.000000000000000000, -1.000000000000000000 ) ) ;
#20589=AXIS2_PLACEMENT_3D ( 'NONE', #10856, #18284, #12698 ) ;
#20620=DIRECTION ( 'NONE',  ( 0.000000000000000000, 0.000000000000000000, 1.000000000000000000 ) ) ;
#20692=ADVANCED_FACE ( 'NONE', ( #16603 ), #21218, .T. ) ;
#20750=CIRCLE ( 'NONE', #12210, 0.2500000000000000000 ) ;
#20892=ORIENTED_EDGE ( 'NONE', *, *, #19171, .T. ) ;
#20917=VERTEX_POINT ( 'NONE', #23994 ) ;
#20996=EDGE_CURVE ( 'NONE', #20917, #20185, #18103, .T. ) ;
#21005=ORIENTED_EDGE ( 'NONE', *, *, #20468, .F. ) ;
#21060=CIRCLE ( 'NONE', #10554, 0.2500000000000000000 ) ;
#21089=ORIENTED_EDGE ( 'NONE', *, *, #2142, .T. ) ;
#21099=CARTESIAN_POINT ( 'NONE',  ( 3.827021247335479543E-17, 0.4997679491924311157, 0.3125000000000001665 ) ) ;
#21106=ORIENTED_EDGE ( 'NONE', *, *, #5635, .T. ) ;
#21112=DIRECTION ( 'NONE',  ( -0.000000000000000000, -1.000000000000000000, -0.000000000000000000 ) ) ;
#21129=CIRCLE ( 'NONE', #2041, 0.2510000000000000009 ) ;
#21212=ORIENTED_EDGE ( 'NONE', *, *, #612, .T. ) ;
#21218=CONICAL_SURFACE ( 'NONE', #11089, 0.2041999999999999926, 0.7853981633974563836 ) ;
#21240=ADVANCED_FACE ( 'NONE', ( #13439 ), #2569, .T. ) ;
#21244=CIRCLE ( 'NONE', #15397, 0.2041999999999999926 ) ;
#21270=DIRECTION ( 'NONE',  ( -0.000000000000000000, 1.000000000000000000, -0.000000000000000000 ) ) ;
#21279=ORIENTED_EDGE ( 'NONE', *, *, #1659, .T. ) ;
#21305=VECTOR ( 'NONE', #17214, 39.37007874015748143 ) ;
#21306=CARTESIAN_POINT ( 'NONE',  ( 0.000000000000000000, 0.4202679491924311561, 0.2499999999999999722 ) ) ;
#21411=CARTESIAN_POINT ( 'NONE',  ( 0.000000000000000000, 0.000000000000000000, 0.000000000000000000 ) ) ;
#21432=CONICAL_SURFACE ( 'NONE', #19863, 0.2500000000000000555, 0.5235987755984723435 ) ;
#21472=DIRECTION ( 'NONE',  ( 0.000000000000000000, 0.000000000000000000, -1.000000000000000000 ) ) ;
#21481=VERTEX_POINT ( 'NONE', #5920 ) ;
#21523=DIRECTION ( 'NONE',  ( -0.000000000000000000, -1.000000000000000000, -0.000000000000000000 ) ) ;
#21551=DIRECTION ( 'NONE',  ( 0.000000000000000000, 0.000000000000000000, 1.000000000000000000 ) ) ;
#21553=ORIENTED_EDGE ( 'NONE', *, *, #15758, .F. ) ;
#21560=AXIS2_PLACEMENT_3D ( 'NONE', #16137, #9660, #14914 ) ;
#21603=LENGTH_MEASURE_WITH_UNIT ( LENGTH_MEASURE( 0.02539999999999999897 ), #17348 );
#21636=CIRCLE ( 'NONE', #9987, 0.2041999999999999926 ) ;
#21678=CARTESIAN_POINT ( 'NONE',  ( 3.061616997868383634E-17, 5.580000000000000959, 0.2500000000000000555 ) ) ;
#21766=DIRECTION ( 'NONE',  ( 0.000000000000000000, 0.000000000000000000, -1.000000000000000000 ) ) ;
#21776=DIRECTION ( 'NONE',  ( 0.000000000000000000, 0.000000000000000000, -1.000000000000000000 ) ) ;
#21783=AXIS2_PLACEMENT_3D ( 'NONE', #3634, #11083, #18513 ) ;
#21793=VERTEX_POINT ( 'NONE', #16277 ) ;
#21811=DIRECTION ( 'NONE',  ( 0.000000000000000000, 0.000000000000000000, 1.000000000000000000 ) ) ;
#21858=EDGE_CURVE ( 'NONE', #409, #18846, #20454, .T. ) ;
#21863=PLANE ( 'NONE',  #10882 ) ;
#21868=ORIENTED_EDGE ( 'NONE', *, *, #23959, .F. ) ;
#21898=AXIS2_PLACEMENT_3D ( 'NONE', #16442, #18749, #20578 ) ;
#21914=CARTESIAN_POINT ( 'NONE',  ( 0.000000000000000000, 6.000000000000000888, -0.3125000000000000555 ) ) ;
#21995=MECHANICAL_CONTEXT ( 'NONE', #2656, 'mechanical' ) ;
#22020=ORIENTED_EDGE ( 'NONE', *, *, #18301, .F. ) ;
#22033=CARTESIAN_POINT ( 'NONE',  ( 0.000000000000000000, 0.4987679491924311148, 0.000000000000000000 ) ) ;
#22047=AXIS2_PLACEMENT_3D ( 'NONE', #1212, #11058, #18486 ) ;
#22067=LINE ( 'NONE', #12227, #11853 ) ;
#22114=VERTEX_POINT ( 'NONE', #19626 ) ;
#22124=ORIENTED_EDGE ( 'NONE', *, *, #5635, .F. ) ;
#22138=EDGE_CURVE ( 'NONE', #13516, #21481, #21244, .T. ) ;
#22139=EDGE_CURVE ( 'NONE', #6959, #21793, #7189, .T. ) ;
#22159=DIRECTION ( 'NONE',  ( -1.000000000000000000, 0.000000000000000000, 0.000000000000000000 ) ) ;
#22179=CIRCLE ( 'NONE', #14810, 0.2499999999999999722 ) ;
#22271=DIRECTION ( 'NONE',  ( -0.000000000000000000, 1.000000000000000000, -0.000000000000000000 ) ) ;
#22282=CARTESIAN_POINT ( 'NONE',  ( 0.000000000000000000, 6.000000000000000888, 0.000000000000000000 ) ) ;
#22292=CIRCLE ( 'NONE', #21898, 0.2501339745962155581 ) ;
#22300=FACE_OUTER_BOUND ( 'NONE', #6730, .T. ) ;
#22332=CYLINDRICAL_SURFACE ( 'NONE', #19820, 0.2500000000000000000 ) ;
#22456=PLANE ( 'NONE',  #9768 ) ;
#22476=VERTEX_POINT ( 'NONE', #15586 ) ;
#22600=ORIENTED_EDGE ( 'NONE', *, *, #6916, .F. ) ;
#22609=CIRCLE ( 'NONE', #16009, 0.3125000000000001665 ) ;
#22636=DIRECTION ( 'NONE',  ( -0.000000000000000000, 1.000000000000000000, -0.000000000000000000 ) ) ;
#22657=EDGE_LOOP ( 'NONE', ( #23947, #2445, #10104, #22020 ) ) ;
#22676=ORIENTED_EDGE ( 'NONE', *, *, #18817, .T. ) ;
#22691=DIRECTION ( 'NONE',  ( 1.000000000000000000, 0.000000000000000000, 1.224646799147353207E-16 ) ) ;
#22714=EDGE_CURVE ( 'NONE', #15814, #20917, #18980, .T. ) ;
#22716=DIRECTION ( 'NONE',  ( 0.000000000000000000, 0.000000000000000000, 1.000000000000000000 ) ) ;
#22733=CIRCLE ( 'NONE', #21560, 0.2041999999999999926 ) ;
#22735=FACE_OUTER_BOUND ( 'NONE', #13598, .T. ) ;
#22748=CIRCLE ( 'NONE', #4448, 0.2500000000000000555 ) ;
#22811=FACE_OUTER_BOUND ( 'NONE', #2678, .T. ) ;
#22900=DIRECTION ( 'NONE',  ( 1.000000000000000000, 0.000000000000000000, -1.224646799147353207E-16 ) ) ;
#22934=CYLINDRICAL_SURFACE ( 'NONE', #15344, 0.2499999999999999722 ) ;
#22945=TOROIDAL_SURFACE ( 'NONE', #21783, 0.2510000000000000009, 0.0009999999999999896125 ) ;
#22967=CARTESIAN_POINT ( 'NONE',  ( 0.000000000000000000, 0.4997679491924311157, 0.000000000000000000 ) ) ;
#22973=ORIENTED_EDGE ( 'NONE', *, *, #19752, .F. ) ;
#22991=ADVANCED_FACE ( 'NONE', ( #7376 ), #10805, .T. ) ;
#22995=DIRECTION ( 'NONE',  ( 0.000000000000000000, 0.000000000000000000, 1.000000000000000000 ) ) ;
#23061=SHAPE_REPRESENTATION_RELATIONSHIP ( 'NONE' , 'NONE' ,  #16955, #8245 ) ;
#23096=AXIS2_PLACEMENT_3D ( 'NONE', #14893, #4264, #19137 ) ;
#23181=DIRECTION ( 'NONE',  ( 0.000000000000000000, 0.000000000000000000, 1.000000000000000000 ) ) ;
#23209=VERTEX_POINT ( 'NONE', #4753 ) ;
#23232=AXIS2_PLACEMENT_3D ( 'NONE', #11251, #14909, #7581 ) ;
#23284=TOROIDAL_SURFACE ( 'NONE', #20569, 0.2510000000000000009, 0.0009999999999999859262 ) ;
#23290=ORIENTED_EDGE ( 'NONE', *, *, #15440, .F. ) ;
#23294=DIRECTION ( 'NONE',  ( 1.000000000000000000, 0.000000000000000000, 0.000000000000000000 ) ) ;
#23423=EDGE_CURVE ( 'NONE', #1686, #11401, #12715, .T. ) ;
#23429=CARTESIAN_POINT ( 'NONE',  ( 0.000000000000000000, 5.500232050807569273, 0.000000000000000000 ) ) ;
#23446=ADVANCED_FACE ( 'NONE', ( #14337 ), #12164, .T. ) ;
#23496=CARTESIAN_POINT ( 'NONE',  ( 0.000000000000000000, 0.4987679491924311148, 0.2500000000000000000 ) ) ;
#23581=DIRECTION ( 'NONE',  ( 0.000000000000000000, 0.000000000000000000, 1.000000000000000000 ) ) ;
#23643=CARTESIAN_POINT ( 'NONE',  ( 3.063257713472607067E-17, 5.580232050807569344, -0.2501339745962155581 ) ) ;
#23649=ADVANCED_FACE ( 'NONE', ( #13362 ), #13250, .T. ) ;
#23666=DIRECTION ( 'NONE',  ( -0.000000000000000000, -1.000000000000000000, -0.000000000000000000 ) ) ;
#23679=DIRECTION ( 'NONE',  ( -0.000000000000000000, -1.000000000000000000, -0.000000000000000000 ) ) ;
#23687=EDGE_CURVE ( 'NONE', #22114, #9682, #21636, .T. ) ;
#23707=CARTESIAN_POINT ( 'NONE',  ( 0.000000000000000000, 5.580000000000000959, 0.000000000000000000 ) ) ;
#23737=ORIENTED_EDGE ( 'NONE', *, *, #23959, .T. ) ;
#23756=DIRECTION ( 'NONE',  ( -0.000000000000000000, -1.000000000000000000, -0.000000000000000000 ) ) ;
#23762=LINE ( 'NONE', #10866, #16123 ) ;
#23776=DIRECTION ( 'NONE',  ( 0.000000000000000000, 0.000000000000000000, 1.000000000000000000 ) ) ;
#23801=DIRECTION ( 'NONE',  ( 0.000000000000000000, 0.000000000000000000, -1.000000000000000000 ) ) ;
#23851=EDGE_CURVE ( 'NONE', #23209, #19709, #4902, .T. ) ;
#23860=ORIENTED_EDGE ( 'NONE', *, *, #18001, .T. ) ;
#23902=EDGE_CURVE ( 'NONE', #14094, #8085, #13820, .T. ) ;
#23947=ORIENTED_EDGE ( 'NONE', *, *, #17389, .T. ) ;
#23948=ORIENTED_EDGE ( 'NONE', *, *, #13525, .F. ) ;
#23959=EDGE_CURVE ( 'NONE', #14094, #4761, #14201, .T. ) ;
#23994=CARTESIAN_POINT ( 'NONE',  ( 0.000000000000000000, 0.4197679491924312112, -0.2501339745962155581 ) ) ;
#23998=DIRECTION ( 'NONE',  ( 0.000000000000000000, 0.000000000000000000, -1.000000000000000000 ) ) ;
#24031=ORIENTED_EDGE ( 'NONE', *, *, #23423, .F. ) ;
#24050=CARTESIAN_POINT ( 'NONE',  ( 0.000000000000000000, 0.000000000000000000, 0.000000000000000000 ) ) ;
#24112=ORIENTED_EDGE ( 'NONE', *, *, #23687, .F. ) ;
#24166=COLOUR_RGB('Light Gray', 0.08235294, 0.09019608, 0.10196078);
#24167=FILL_AREA_STYLE_COLOUR('',#24166);
#24168=FILL_AREA_STYLE('',(#24167));
#24169=SURFACE_STYLE_FILL_AREA(#24168);
#24170=SURFACE_SIDE_STYLE('',(#24169));
#24171=SURFACE_STYLE_USAGE(.BOTH.,#24170);
#24172=PRESENTATION_STYLE_ASSIGNMENT((#24171));
#24186=STYLED_ITEM('',(#24172),#8780);
#24187=MECHANICAL_DESIGN_GEOMETRIC_PRESENTATION_REPRESENTATION('',(#24186),#14988);
ENDSEC;
END-ISO-10303-21;
